ISO-10303-21;
HEADER;
/* Generated by software containing ST-Developer
 * from STEP Tools, Inc. (www.steptools.com) 
 */

FILE_DESCRIPTION(
/* description */ ('Bin tilter linkage'),
/* implementation_level */ '2;1');

FILE_NAME(
/* name */ 'Screw bearing keeper (1).step',
/* time_stamp */ '2026-10-28T03:26:24-07:00',
/* author */ (''),
/* organization */ (''),
/* preprocessor_version */ 'ST-DEVELOPER v20.2',
/* originating_system */ 'Autodesk Translation Framework v15.17.0.0',
/* authorisation */ '');

FILE_SCHEMA (('AUTOMOTIVE_DESIGN { 1 0 10303 214 3 1 1 }'));
ENDSEC;

DATA;
#10=MECHANICAL_DESIGN_GEOMETRIC_PRESENTATION_REPRESENTATION('',(#879),#23728);
#667=SHAPE_REPRESENTATION_RELATIONSHIP('SRR','None',#24131,#773);
#773=ADVANCED_BREP_SHAPE_REPRESENTATION('',(#993),#23631);
#879=STYLED_ITEM('',(#24772),#993);
#993=MANIFOLD_SOLID_BREP('Body1',#12409);
#1195=FACE_BOUND('',#2931,.T.);
#1196=FACE_BOUND('',#2932,.T.);
#1197=FACE_BOUND('',#2933,.T.);
#1198=FACE_BOUND('',#2938,.T.);
#1199=FACE_BOUND('',#2939,.T.);
#1200=FACE_BOUND('',#2940,.T.);
#1569=PLANE('',#14007);
#1570=PLANE('',#14017);
#2041=FACE_OUTER_BOUND('',#2926,.T.);
#2042=FACE_OUTER_BOUND('',#2927,.T.);
#2043=FACE_OUTER_BOUND('',#2928,.T.);
#2044=FACE_OUTER_BOUND('',#2929,.T.);
#2045=FACE_OUTER_BOUND('',#2930,.T.);
#2046=FACE_OUTER_BOUND('',#2934,.T.);
#2047=FACE_OUTER_BOUND('',#2935,.T.);
#2048=FACE_OUTER_BOUND('',#2936,.T.);
#2049=FACE_OUTER_BOUND('',#2937,.T.);
#2926=EDGE_LOOP('',(#9015,#9016,#9017,#9018));
#2927=EDGE_LOOP('',(#9019,#9020,#9021,#9022));
#2928=EDGE_LOOP('',(#9023,#9024,#9025,#9026));
#2929=EDGE_LOOP('',(#9027,#9028,#9029,#9030));
#2930=EDGE_LOOP('',(#9031,#9032,#9033,#9034));
#2931=EDGE_LOOP('',(#9035));
#2932=EDGE_LOOP('',(#9036));
#2933=EDGE_LOOP('',(#9037));
#2934=EDGE_LOOP('',(#9038,#9039,#9040,#9041));
#2935=EDGE_LOOP('',(#9042,#9043,#9044,#9045));
#2936=EDGE_LOOP('',(#9046,#9047,#9048,#9049));
#2937=EDGE_LOOP('',(#9050,#9051,#9052,#9053));
#2938=EDGE_LOOP('',(#9054));
#2939=EDGE_LOOP('',(#9055));
#2940=EDGE_LOOP('',(#9056));
#4022=LINE('',#20455,#4697);
#4023=LINE('',#20461,#4698);
#4024=LINE('',#20466,#4699);
#4025=LINE('',#20470,#4700);
#4026=LINE('',#20475,#4701);
#4027=LINE('',#20479,#4702);
#4028=LINE('',#20492,#4703);
#4697=VECTOR('',#16289,0.225);
#4698=VECTOR('',#16296,0.225);
#4699=VECTOR('',#16301,1.);
#4700=VECTOR('',#16304,1.);
#4701=VECTOR('',#16309,1.);
#4702=VECTOR('',#16312,1.);
#4703=VECTOR('',#16333,1.02);
#5347=CIRCLE('',#13996,0.225);
#5348=CIRCLE('',#13997,0.225);
#5349=CIRCLE('',#13999,0.225);
#5350=CIRCLE('',#14000,0.225);
#5351=CIRCLE('',#14002,0.61);
#5352=CIRCLE('',#14003,0.61);
#5353=CIRCLE('',#14005,0.61);
#5354=CIRCLE('',#14006,0.61);
#5355=CIRCLE('',#14008,2.1);
#5356=CIRCLE('',#14009,2.1);
#5357=CIRCLE('',#14010,1.02);
#5358=CIRCLE('',#14012,2.1);
#5359=CIRCLE('',#14014,2.1);
#5360=CIRCLE('',#14016,1.02);
#6171=VERTEX_POINT('',#20452);
#6172=VERTEX_POINT('',#20454);
#6173=VERTEX_POINT('',#20458);
#6174=VERTEX_POINT('',#20460);
#6175=VERTEX_POINT('',#20464);
#6176=VERTEX_POINT('',#20465);
#6177=VERTEX_POINT('',#20467);
#6178=VERTEX_POINT('',#20469);
#6179=VERTEX_POINT('',#20473);
#6180=VERTEX_POINT('',#20474);
#6181=VERTEX_POINT('',#20476);
#6182=VERTEX_POINT('',#20478);
#6183=VERTEX_POINT('',#20484);
#6184=VERTEX_POINT('',#20491);
#7247=EDGE_CURVE('',#6171,#6171,#5347,.T.);
#7248=EDGE_CURVE('',#6171,#6172,#4022,.T.);
#7249=EDGE_CURVE('',#6172,#6172,#5348,.T.);
#7250=EDGE_CURVE('',#6173,#6173,#5349,.T.);
#7251=EDGE_CURVE('',#6173,#6174,#4023,.T.);
#7252=EDGE_CURVE('',#6174,#6174,#5350,.T.);
#7253=EDGE_CURVE('',#6175,#6176,#4024,.T.);
#7254=EDGE_CURVE('',#6177,#6175,#5351,.T.);
#7255=EDGE_CURVE('',#6178,#6177,#4025,.T.);
#7256=EDGE_CURVE('',#6176,#6178,#5352,.T.);
#7257=EDGE_CURVE('',#6179,#6180,#4026,.T.);
#7258=EDGE_CURVE('',#6181,#6179,#5353,.T.);
#7259=EDGE_CURVE('',#6182,#6181,#4027,.T.);
#7260=EDGE_CURVE('',#6180,#6182,#5354,.T.);
#7261=EDGE_CURVE('',#6175,#6181,#5355,.T.);
#7262=EDGE_CURVE('',#6179,#6177,#5356,.T.);
#7263=EDGE_CURVE('',#6183,#6183,#5357,.T.);
#7264=EDGE_CURVE('',#6176,#6182,#5358,.T.);
#7265=EDGE_CURVE('',#6180,#6178,#5359,.T.);
#7266=EDGE_CURVE('',#6183,#6184,#4028,.T.);
#7267=EDGE_CURVE('',#6184,#6184,#5360,.T.);
#9015=ORIENTED_EDGE('',*,*,#7247,.F.);
#9016=ORIENTED_EDGE('',*,*,#7248,.T.);
#9017=ORIENTED_EDGE('',*,*,#7249,.F.);
#9018=ORIENTED_EDGE('',*,*,#7248,.F.);
#9019=ORIENTED_EDGE('',*,*,#7250,.F.);
#9020=ORIENTED_EDGE('',*,*,#7251,.T.);
#9021=ORIENTED_EDGE('',*,*,#7252,.F.);
#9022=ORIENTED_EDGE('',*,*,#7251,.F.);
#9023=ORIENTED_EDGE('',*,*,#7253,.F.);
#9024=ORIENTED_EDGE('',*,*,#7254,.F.);
#9025=ORIENTED_EDGE('',*,*,#7255,.F.);
#9026=ORIENTED_EDGE('',*,*,#7256,.F.);
#9027=ORIENTED_EDGE('',*,*,#7257,.F.);
#9028=ORIENTED_EDGE('',*,*,#7258,.F.);
#9029=ORIENTED_EDGE('',*,*,#7259,.F.);
#9030=ORIENTED_EDGE('',*,*,#7260,.F.);
#9031=ORIENTED_EDGE('',*,*,#7254,.T.);
#9032=ORIENTED_EDGE('',*,*,#7261,.T.);
#9033=ORIENTED_EDGE('',*,*,#7258,.T.);
#9034=ORIENTED_EDGE('',*,*,#7262,.T.);
#9035=ORIENTED_EDGE('',*,*,#7249,.T.);
#9036=ORIENTED_EDGE('',*,*,#7252,.T.);
#9037=ORIENTED_EDGE('',*,*,#7263,.T.);
#9038=ORIENTED_EDGE('',*,*,#7253,.T.);
#9039=ORIENTED_EDGE('',*,*,#7264,.T.);
#9040=ORIENTED_EDGE('',*,*,#7259,.T.);
#9041=ORIENTED_EDGE('',*,*,#7261,.F.);
#9042=ORIENTED_EDGE('',*,*,#7255,.T.);
#9043=ORIENTED_EDGE('',*,*,#7262,.F.);
#9044=ORIENTED_EDGE('',*,*,#7257,.T.);
#9045=ORIENTED_EDGE('',*,*,#7265,.T.);
#9046=ORIENTED_EDGE('',*,*,#7263,.F.);
#9047=ORIENTED_EDGE('',*,*,#7266,.T.);
#9048=ORIENTED_EDGE('',*,*,#7267,.T.);
#9049=ORIENTED_EDGE('',*,*,#7266,.F.);
#9050=ORIENTED_EDGE('',*,*,#7256,.T.);
#9051=ORIENTED_EDGE('',*,*,#7265,.F.);
#9052=ORIENTED_EDGE('',*,*,#7260,.T.);
#9053=ORIENTED_EDGE('',*,*,#7264,.F.);
#9054=ORIENTED_EDGE('',*,*,#7247,.T.);
#9055=ORIENTED_EDGE('',*,*,#7250,.T.);
#9056=ORIENTED_EDGE('',*,*,#7267,.F.);
#11341=CYLINDRICAL_SURFACE('',#13995,0.225);
#11342=CYLINDRICAL_SURFACE('',#13998,0.225);
#11343=CYLINDRICAL_SURFACE('',#14001,0.61);
#11344=CYLINDRICAL_SURFACE('',#14004,0.61);
#11345=CYLINDRICAL_SURFACE('',#14011,2.1);
#11346=CYLINDRICAL_SURFACE('',#14013,2.1);
#11347=CYLINDRICAL_SURFACE('',#14015,1.02);
#11766=ADVANCED_FACE('',(#2041),#11341,.F.);
#11767=ADVANCED_FACE('',(#2042),#11342,.F.);
#11768=ADVANCED_FACE('',(#2043),#11343,.F.);
#11769=ADVANCED_FACE('',(#2044),#11344,.F.);
#11770=ADVANCED_FACE('',(#2045,#1195,#1196,#1197),#1569,.T.);
#11771=ADVANCED_FACE('',(#2046),#11345,.T.);
#11772=ADVANCED_FACE('',(#2047),#11346,.T.);
#11773=ADVANCED_FACE('',(#2048),#11347,.F.);
#11774=ADVANCED_FACE('',(#2049,#1198,#1199,#1200),#1570,.F.);
#12409=CLOSED_SHELL('',(#11766,#11767,#11768,#11769,#11770,#11771,#11772,
#11773,#11774));
#13994=AXIS2_PLACEMENT_3D('',#20450,#16283,#16284);
#13995=AXIS2_PLACEMENT_3D('',#20451,#16285,#16286);
#13996=AXIS2_PLACEMENT_3D('',#20453,#16287,#16288);
#13997=AXIS2_PLACEMENT_3D('',#20456,#16290,#16291);
#13998=AXIS2_PLACEMENT_3D('',#20457,#16292,#16293);
#13999=AXIS2_PLACEMENT_3D('',#20459,#16294,#16295);
#14000=AXIS2_PLACEMENT_3D('',#20462,#16297,#16298);
#14001=AXIS2_PLACEMENT_3D('',#20463,#16299,#16300);
#14002=AXIS2_PLACEMENT_3D('',#20468,#16302,#16303);
#14003=AXIS2_PLACEMENT_3D('',#20471,#16305,#16306);
#14004=AXIS2_PLACEMENT_3D('',#20472,#16307,#16308);
#14005=AXIS2_PLACEMENT_3D('',#20477,#16310,#16311);
#14006=AXIS2_PLACEMENT_3D('',#20480,#16313,#16314);
#14007=AXIS2_PLACEMENT_3D('',#20481,#16315,#16316);
#14008=AXIS2_PLACEMENT_3D('',#20482,#16317,#16318);
#14009=AXIS2_PLACEMENT_3D('',#20483,#16319,#16320);
#14010=AXIS2_PLACEMENT_3D('',#20485,#16321,#16322);
#14011=AXIS2_PLACEMENT_3D('',#20486,#16323,#16324);
#14012=AXIS2_PLACEMENT_3D('',#20487,#16325,#16326);
#14013=AXIS2_PLACEMENT_3D('',#20488,#16327,#16328);
#14014=AXIS2_PLACEMENT_3D('',#20489,#16329,#16330);
#14015=AXIS2_PLACEMENT_3D('',#20490,#16331,#16332);
#14016=AXIS2_PLACEMENT_3D('',#20493,#16334,#16335);
#14017=AXIS2_PLACEMENT_3D('',#20494,#16336,#16337);
#16283=DIRECTION('axis',(0.,0.,1.));
#16284=DIRECTION('refdir',(1.,0.,0.));
#16285=DIRECTION('center_axis',(1.,0.,0.));
#16286=DIRECTION('ref_axis',(0.,0.,-1.));
#16287=DIRECTION('center_axis',(1.,0.,0.));
#16288=DIRECTION('ref_axis',(0.,0.,-1.));
#16289=DIRECTION('',(1.,0.,0.));
#16290=DIRECTION('center_axis',(-1.,0.,0.));
#16291=DIRECTION('ref_axis',(0.,0.,-1.));
#16292=DIRECTION('center_axis',(1.,0.,0.));
#16293=DIRECTION('ref_axis',(0.,0.,-1.));
#16294=DIRECTION('center_axis',(1.,0.,0.));
#16295=DIRECTION('ref_axis',(0.,0.,-1.));
#16296=DIRECTION('',(1.,0.,0.));
#16297=DIRECTION('center_axis',(-1.,0.,0.));
#16298=DIRECTION('ref_axis',(0.,0.,-1.));
#16299=DIRECTION('center_axis',(1.,0.,0.));
#16300=DIRECTION('ref_axis',(0.,0.,-1.));
#16301=DIRECTION('',(-1.,0.,0.));
#16302=DIRECTION('center_axis',(-1.,0.,0.));
#16303=DIRECTION('ref_axis',(0.,0.,-1.));
#16304=DIRECTION('',(1.,0.,0.));
#16305=DIRECTION('center_axis',(1.,0.,0.));
#16306=DIRECTION('ref_axis',(0.,0.,-1.));
#16307=DIRECTION('center_axis',(1.,0.,0.));
#16308=DIRECTION('ref_axis',(0.,0.,-1.));
#16309=DIRECTION('',(-1.,0.,0.));
#16310=DIRECTION('center_axis',(-1.,0.,0.));
#16311=DIRECTION('ref_axis',(0.,0.,-1.));
#16312=DIRECTION('',(1.,0.,0.));
#16313=DIRECTION('center_axis',(1.,0.,0.));
#16314=DIRECTION('ref_axis',(0.,0.,-1.));
#16315=DIRECTION('center_axis',(1.,0.,0.));
#16316=DIRECTION('ref_axis',(0.,0.,-1.));
#16317=DIRECTION('center_axis',(1.,0.,0.));
#16318=DIRECTION('ref_axis',(0.,0.,-1.));
#16319=DIRECTION('center_axis',(1.,0.,0.));
#16320=DIRECTION('ref_axis',(0.,0.,-1.));
#16321=DIRECTION('center_axis',(-1.,0.,0.));
#16322=DIRECTION('ref_axis',(0.,0.,-1.));
#16323=DIRECTION('center_axis',(1.,0.,0.));
#16324=DIRECTION('ref_axis',(0.,0.,-1.));
#16325=DIRECTION('center_axis',(1.,0.,0.));
#16326=DIRECTION('ref_axis',(0.,0.,-1.));
#16327=DIRECTION('center_axis',(1.,0.,0.));
#16328=DIRECTION('ref_axis',(0.,-1.22464679914735E-16,1.));
#16329=DIRECTION('center_axis',(1.,0.,0.));
#16330=DIRECTION('ref_axis',(0.,0.,-1.));
#16331=DIRECTION('center_axis',(1.,0.,0.));
#16332=DIRECTION('ref_axis',(0.,0.,-1.));
#16333=DIRECTION('',(-1.,0.,0.));
#16334=DIRECTION('center_axis',(-1.,0.,0.));
#16335=DIRECTION('ref_axis',(0.,0.,-1.));
#16336=DIRECTION('center_axis',(1.,0.,0.));
#16337=DIRECTION('ref_axis',(0.,0.,-1.));
#20450=CARTESIAN_POINT('',(0.,0.,0.));
#20451=CARTESIAN_POINT('Origin',(-9.1,-4.5,9.85));
#20452=CARTESIAN_POINT('',(-9.,-4.5,10.075));
#20453=CARTESIAN_POINT('Origin',(-9.,-4.5,9.85));
#20454=CARTESIAN_POINT('',(-8.8,-4.5,10.075));
#20455=CARTESIAN_POINT('',(-9.1,-4.5,10.075));
#20456=CARTESIAN_POINT('Origin',(-8.8,-4.5,9.85));
#20457=CARTESIAN_POINT('Origin',(-9.1,-4.5,6.15));
#20458=CARTESIAN_POINT('',(-9.,-4.5,6.375));
#20459=CARTESIAN_POINT('Origin',(-9.,-4.5,6.15));
#20460=CARTESIAN_POINT('',(-8.8,-4.5,6.375));
#20461=CARTESIAN_POINT('',(-9.1,-4.5,6.375));
#20462=CARTESIAN_POINT('Origin',(-8.8,-4.5,6.15));
#20463=CARTESIAN_POINT('Origin',(-9.1,-7.,8.));
#20464=CARTESIAN_POINT('',(-8.8,-6.55758,7.58004221212127));
#20465=CARTESIAN_POINT('',(-9.,-6.55758,7.58004221212127));
#20466=CARTESIAN_POINT('',(-9.1,-6.55758,7.58004221212127));
#20467=CARTESIAN_POINT('',(-8.8,-6.55758,8.41995778787873));
#20468=CARTESIAN_POINT('Origin',(-8.8,-7.,8.));
#20469=CARTESIAN_POINT('',(-9.,-6.55758,8.41995778787873));
#20470=CARTESIAN_POINT('',(-9.1,-6.55758,8.41995778787873));
#20471=CARTESIAN_POINT('Origin',(-9.,-7.,8.));
#20472=CARTESIAN_POINT('Origin',(-9.1,-2.,8.));
#20473=CARTESIAN_POINT('',(-8.8,-2.44242,8.41995778787873));
#20474=CARTESIAN_POINT('',(-9.,-2.44242,8.41995778787873));
#20475=CARTESIAN_POINT('',(-9.1,-2.44242,8.41995778787873));
#20476=CARTESIAN_POINT('',(-8.8,-2.44242,7.58004221212127));
#20477=CARTESIAN_POINT('Origin',(-8.8,-2.,8.));
#20478=CARTESIAN_POINT('',(-9.,-2.44242,7.58004221212127));
#20479=CARTESIAN_POINT('',(-9.1,-2.44242,7.58004221212127));
#20480=CARTESIAN_POINT('Origin',(-9.,-2.,8.));
#20481=CARTESIAN_POINT('Origin',(-8.8,-4.5,8.));
#20482=CARTESIAN_POINT('Origin',(-8.8,-4.5,8.));
#20483=CARTESIAN_POINT('Origin',(-8.8,-4.5,8.));
#20484=CARTESIAN_POINT('',(-8.8,-4.5,9.02));
#20485=CARTESIAN_POINT('Origin',(-8.8,-4.5,8.));
#20486=CARTESIAN_POINT('Origin',(-9.,-4.5,8.));
#20487=CARTESIAN_POINT('Origin',(-9.,-4.5,8.));
#20488=CARTESIAN_POINT('Origin',(-9.,-4.5,8.));
#20489=CARTESIAN_POINT('Origin',(-9.,-4.5,8.));
#20490=CARTESIAN_POINT('Origin',(-9.,-4.5,8.));
#20491=CARTESIAN_POINT('',(-9.,-4.5,9.02));
#20492=CARTESIAN_POINT('',(-9.,-4.5,9.02));
#20493=CARTESIAN_POINT('Origin',(-9.,-4.5,8.));
#20494=CARTESIAN_POINT('Origin',(-9.,-4.5,8.));
#23514=UNCERTAINTY_MEASURE_WITH_UNIT(LENGTH_MEASURE(0.001),#23729,
'DISTANCE_ACCURACY_VALUE',
'Maximum model space distance between geometric entities at asserted c
onnectivities');
#23611=UNCERTAINTY_MEASURE_WITH_UNIT(LENGTH_MEASURE(0.001),#23729,
'DISTANCE_ACCURACY_VALUE',
'Maximum model space distance between geometric entities at asserted c
onnectivities');
#23631=(
GEOMETRIC_REPRESENTATION_CONTEXT(3)
GLOBAL_UNCERTAINTY_ASSIGNED_CONTEXT((#23514))
GLOBAL_UNIT_ASSIGNED_CONTEXT((#23729,#23731,#23732))
REPRESENTATION_CONTEXT('','3D')
);
#23728=(
GEOMETRIC_REPRESENTATION_CONTEXT(3)
GLOBAL_UNCERTAINTY_ASSIGNED_CONTEXT((#23611))
GLOBAL_UNIT_ASSIGNED_CONTEXT((#23729,#23731,#23732))
REPRESENTATION_CONTEXT('','3D')
);
#23729=(
LENGTH_UNIT()
NAMED_UNIT(*)
SI_UNIT(.CENTI.,.METRE.)
);
#23731=(
NAMED_UNIT(*)
PLANE_ANGLE_UNIT()
SI_UNIT($,.RADIAN.)
);
#23732=(
NAMED_UNIT(*)
SI_UNIT($,.STERADIAN.)
SOLID_ANGLE_UNIT()
);
#23752=SHAPE_DEFINITION_REPRESENTATION(#23868,#24131);
#23868=PRODUCT_DEFINITION_SHAPE('',$,#24248);
#24131=SHAPE_REPRESENTATION('',(#13994),#23631);
#24228=PRODUCT_DEFINITION_CONTEXT('part definition',#24578,'design');
#24248=PRODUCT_DEFINITION('Screw bearing keeper (1)',
'Screw bearing keeper (1)',#24364,#24228);
#24364=PRODUCT_DEFINITION_FORMATION('',$,#24599);
#24578=APPLICATION_CONTEXT(
'Core Data for Automotive Mechanical Design Process');
#24579=PRODUCT_CONTEXT('part definition',#24578,'mechanical');
#24599=PRODUCT('Screw bearing keeper (1)','Screw bearing keeper (1)',
'Screw bearing keeper (1)',(#24579));
#24766=COLOUR_RGB('Black',0.12,0.14,0.17);
#24767=FILL_AREA_STYLE_COLOUR('',#24766);
#24768=FILL_AREA_STYLE('',(#24767));
#24769=SURFACE_STYLE_FILL_AREA(#24768);
#24770=SURFACE_SIDE_STYLE('',(#24769));
#24771=SURFACE_STYLE_USAGE(.BOTH.,#24770);
#24772=PRESENTATION_STYLE_ASSIGNMENT((#24771));
ENDSEC;
END-ISO-10303-21;
